ISO-10303-21;
HEADER;
/* Generated by software containing ST-Developer
 * from STEP Tools, Inc. (www.steptools.com) 
 */

FILE_DESCRIPTION(
/* description */ ('Line shaft on three pillow blocks'),
/* implementation_level */ '2;1');

FILE_NAME(
/* name */ 'M8x25 Bolt.step',
/* time_stamp */ '2026-10-27T10:49:19-07:00',
/* author */ (''),
/* organization */ (''),
/* preprocessor_version */ 'ST-DEVELOPER v20.2',
/* originating_system */ 'Autodesk Translation Framework v15.17.0.0',
/* authorisation */ '');

FILE_SCHEMA (('AUTOMOTIVE_DESIGN { 1 0 10303 214 3 1 1 }'));
ENDSEC;

DATA;
#10=MECHANICAL_DESIGN_GEOMETRIC_PRESENTATION_REPRESENTATION('',(#355),#8377);
#266=ORIENTED_CLOSED_SHELL('',*,#4342,.F.);
#272=CONICAL_SURFACE('',#4919,0.625,0.785398163397448);
#273=CONICAL_SURFACE('',#4923,0.635,0.785398163397449);
#274=CONICAL_SURFACE('',#4927,0.41,0.463647609000806);
#282=BREP_WITH_VOIDS('Body1',#4343,(#266));
#300=SHAPE_REPRESENTATION_RELATIONSHIP('SRR','None',#8516,#327);
#327=ADVANCED_BREP_SHAPE_REPRESENTATION('',(#282),#8365);
#355=STYLED_ITEM('',(#8725),#282);
#461=FACE_BOUND('',#1128,.T.);
#573=PLANE('',#4907);
#574=PLANE('',#4908);
#575=PLANE('',#4909);
#576=PLANE('',#4910);
#577=PLANE('',#4911);
#578=PLANE('',#4912);
#579=PLANE('',#4913);
#580=PLANE('',#4914);
#581=PLANE('',#4915);
#582=PLANE('',#4917);
#583=PLANE('',#4925);
#792=FACE_OUTER_BOUND('',#1114,.T.);
#793=FACE_OUTER_BOUND('',#1115,.T.);
#794=FACE_OUTER_BOUND('',#1116,.T.);
#795=FACE_OUTER_BOUND('',#1117,.T.);
#796=FACE_OUTER_BOUND('',#1118,.T.);
#797=FACE_OUTER_BOUND('',#1119,.T.);
#798=FACE_OUTER_BOUND('',#1120,.T.);
#799=FACE_OUTER_BOUND('',#1121,.T.);
#800=FACE_OUTER_BOUND('',#1122,.T.);
#801=FACE_OUTER_BOUND('',#1123,.T.);
#802=FACE_OUTER_BOUND('',#1124,.T.);
#803=FACE_OUTER_BOUND('',#1125,.T.);
#804=FACE_OUTER_BOUND('',#1126,.T.);
#805=FACE_OUTER_BOUND('',#1127,.T.);
#806=FACE_OUTER_BOUND('',#1129,.T.);
#807=FACE_OUTER_BOUND('',#1130,.T.);
#1114=EDGE_LOOP('',(#3525,#3526,#3527,#3528));
#1115=EDGE_LOOP('',(#3529,#3530,#3531,#3532));
#1116=EDGE_LOOP('',(#3533,#3534,#3535,#3536));
#1117=EDGE_LOOP('',(#3537,#3538,#3539,#3540));
#1118=EDGE_LOOP('',(#3541,#3542,#3543,#3544));
#1119=EDGE_LOOP('',(#3545,#3546,#3547,#3548));
#1120=EDGE_LOOP('',(#3549,#3550,#3551,#3552,#3553,#3554));
#1121=EDGE_LOOP('',(#3555,#3556,#3557,#3558,#3559,#3560));
#1122=EDGE_LOOP('',(#3561));
#1123=EDGE_LOOP('',(#3562));
#1124=EDGE_LOOP('',(#3563,#3564,#3565,#3566));
#1125=EDGE_LOOP('',(#3567,#3568,#3569,#3570));
#1126=EDGE_LOOP('',(#3571,#3572,#3573,#3574));
#1127=EDGE_LOOP('',(#3575));
#1128=EDGE_LOOP('',(#3576));
#1129=EDGE_LOOP('',(#3577,#3578,#3579,#3580));
#1130=EDGE_LOOP('',(#3581,#3582,#3583,#3584));
#1425=LINE('',#7522,#1752);
#1426=LINE('',#7524,#1753);
#1427=LINE('',#7526,#1754);
#1428=LINE('',#7527,#1755);
#1429=LINE('',#7530,#1756);
#1430=LINE('',#7532,#1757);
#1431=LINE('',#7533,#1758);
#1432=LINE('',#7536,#1759);
#1433=LINE('',#7538,#1760);
#1434=LINE('',#7539,#1761);
#1435=LINE('',#7542,#1762);
#1436=LINE('',#7544,#1763);
#1437=LINE('',#7545,#1764);
#1438=LINE('',#7548,#1765);
#1439=LINE('',#7550,#1766);
#1440=LINE('',#7551,#1767);
#1441=LINE('',#7553,#1768);
#1442=LINE('',#7554,#1769);
#1443=LINE('',#7566,#1770);
#1444=LINE('',#7570,#1771);
#1445=LINE('',#7574,#1772);
#1446=LINE('',#7581,#1773);
#1447=LINE('',#7583,#1774);
#1752=VECTOR('',#5828,1.);
#1753=VECTOR('',#5829,1.);
#1754=VECTOR('',#5830,1.);
#1755=VECTOR('',#5831,1.);
#1756=VECTOR('',#5834,1.);
#1757=VECTOR('',#5835,1.);
#1758=VECTOR('',#5836,1.);
#1759=VECTOR('',#5839,1.);
#1760=VECTOR('',#5840,1.);
#1761=VECTOR('',#5841,1.);
#1762=VECTOR('',#5844,1.);
#1763=VECTOR('',#5845,1.);
#1764=VECTOR('',#5846,1.);
#1765=VECTOR('',#5849,1.);
#1766=VECTOR('',#5850,1.);
#1767=VECTOR('',#5851,1.);
#1768=VECTOR('',#5854,1.);
#1769=VECTOR('',#5855,1.);
#1770=VECTOR('',#5872,0.625);
#1771=VECTOR('',#5877,0.65);
#1772=VECTOR('',#5882,0.635);
#1773=VECTOR('',#5891,0.41);
#1774=VECTOR('',#5894,0.4);
#2003=CIRCLE('',#4916,0.3933);
#2004=CIRCLE('',#4918,0.6);
#2005=CIRCLE('',#4920,0.65);
#2006=CIRCLE('',#4922,0.65);
#2007=CIRCLE('',#4924,0.62);
#2008=CIRCLE('',#4926,0.42);
#2009=CIRCLE('',#4928,0.3933);
#2266=VERTEX_POINT('',#7520);
#2267=VERTEX_POINT('',#7521);
#2268=VERTEX_POINT('',#7523);
#2269=VERTEX_POINT('',#7525);
#2270=VERTEX_POINT('',#7529);
#2271=VERTEX_POINT('',#7531);
#2272=VERTEX_POINT('',#7535);
#2273=VERTEX_POINT('',#7537);
#2274=VERTEX_POINT('',#7541);
#2275=VERTEX_POINT('',#7543);
#2276=VERTEX_POINT('',#7547);
#2277=VERTEX_POINT('',#7549);
#2278=VERTEX_POINT('',#7558);
#2279=VERTEX_POINT('',#7561);
#2280=VERTEX_POINT('',#7564);
#2281=VERTEX_POINT('',#7568);
#2282=VERTEX_POINT('',#7572);
#2283=VERTEX_POINT('',#7576);
#2284=VERTEX_POINT('',#7579);
#2711=EDGE_CURVE('',#2266,#2267,#1425,.T.);
#2712=EDGE_CURVE('',#2267,#2268,#1426,.T.);
#2713=EDGE_CURVE('',#2268,#2269,#1427,.T.);
#2714=EDGE_CURVE('',#2266,#2269,#1428,.T.);
#2715=EDGE_CURVE('',#2267,#2270,#1429,.T.);
#2716=EDGE_CURVE('',#2270,#2271,#1430,.T.);
#2717=EDGE_CURVE('',#2271,#2268,#1431,.T.);
#2718=EDGE_CURVE('',#2270,#2272,#1432,.T.);
#2719=EDGE_CURVE('',#2272,#2273,#1433,.T.);
#2720=EDGE_CURVE('',#2273,#2271,#1434,.T.);
#2721=EDGE_CURVE('',#2272,#2274,#1435,.T.);
#2722=EDGE_CURVE('',#2274,#2275,#1436,.T.);
#2723=EDGE_CURVE('',#2275,#2273,#1437,.T.);
#2724=EDGE_CURVE('',#2274,#2276,#1438,.T.);
#2725=EDGE_CURVE('',#2276,#2277,#1439,.T.);
#2726=EDGE_CURVE('',#2277,#2275,#1440,.T.);
#2727=EDGE_CURVE('',#2276,#2266,#1441,.T.);
#2728=EDGE_CURVE('',#2269,#2277,#1442,.T.);
#2729=EDGE_CURVE('',#2278,#2278,#2003,.T.);
#2730=EDGE_CURVE('',#2279,#2279,#2004,.T.);
#2731=EDGE_CURVE('',#2280,#2280,#2005,.T.);
#2732=EDGE_CURVE('',#2280,#2279,#1443,.T.);
#2733=EDGE_CURVE('',#2281,#2281,#2006,.T.);
#2734=EDGE_CURVE('',#2281,#2280,#1444,.T.);
#2735=EDGE_CURVE('',#2282,#2282,#2007,.T.);
#2736=EDGE_CURVE('',#2282,#2281,#1445,.T.);
#2737=EDGE_CURVE('',#2283,#2283,#2008,.T.);
#2738=EDGE_CURVE('',#2284,#2284,#2009,.F.);
#2739=EDGE_CURVE('',#2284,#2283,#1446,.T.);
#2740=EDGE_CURVE('',#2278,#2284,#1447,.T.);
#3525=ORIENTED_EDGE('',*,*,#2711,.T.);
#3526=ORIENTED_EDGE('',*,*,#2712,.T.);
#3527=ORIENTED_EDGE('',*,*,#2713,.T.);
#3528=ORIENTED_EDGE('',*,*,#2714,.F.);
#3529=ORIENTED_EDGE('',*,*,#2715,.T.);
#3530=ORIENTED_EDGE('',*,*,#2716,.T.);
#3531=ORIENTED_EDGE('',*,*,#2717,.T.);
#3532=ORIENTED_EDGE('',*,*,#2712,.F.);
#3533=ORIENTED_EDGE('',*,*,#2718,.T.);
#3534=ORIENTED_EDGE('',*,*,#2719,.T.);
#3535=ORIENTED_EDGE('',*,*,#2720,.T.);
#3536=ORIENTED_EDGE('',*,*,#2716,.F.);
#3537=ORIENTED_EDGE('',*,*,#2721,.T.);
#3538=ORIENTED_EDGE('',*,*,#2722,.T.);
#3539=ORIENTED_EDGE('',*,*,#2723,.T.);
#3540=ORIENTED_EDGE('',*,*,#2719,.F.);
#3541=ORIENTED_EDGE('',*,*,#2724,.T.);
#3542=ORIENTED_EDGE('',*,*,#2725,.T.);
#3543=ORIENTED_EDGE('',*,*,#2726,.T.);
#3544=ORIENTED_EDGE('',*,*,#2722,.F.);
#3545=ORIENTED_EDGE('',*,*,#2727,.T.);
#3546=ORIENTED_EDGE('',*,*,#2714,.T.);
#3547=ORIENTED_EDGE('',*,*,#2728,.T.);
#3548=ORIENTED_EDGE('',*,*,#2725,.F.);
#3549=ORIENTED_EDGE('',*,*,#2727,.F.);
#3550=ORIENTED_EDGE('',*,*,#2724,.F.);
#3551=ORIENTED_EDGE('',*,*,#2721,.F.);
#3552=ORIENTED_EDGE('',*,*,#2718,.F.);
#3553=ORIENTED_EDGE('',*,*,#2715,.F.);
#3554=ORIENTED_EDGE('',*,*,#2711,.F.);
#3555=ORIENTED_EDGE('',*,*,#2728,.F.);
#3556=ORIENTED_EDGE('',*,*,#2713,.F.);
#3557=ORIENTED_EDGE('',*,*,#2717,.F.);
#3558=ORIENTED_EDGE('',*,*,#2720,.F.);
#3559=ORIENTED_EDGE('',*,*,#2723,.F.);
#3560=ORIENTED_EDGE('',*,*,#2726,.F.);
#3561=ORIENTED_EDGE('',*,*,#2729,.F.);
#3562=ORIENTED_EDGE('',*,*,#2730,.F.);
#3563=ORIENTED_EDGE('',*,*,#2731,.F.);
#3564=ORIENTED_EDGE('',*,*,#2732,.T.);
#3565=ORIENTED_EDGE('',*,*,#2730,.T.);
#3566=ORIENTED_EDGE('',*,*,#2732,.F.);
#3567=ORIENTED_EDGE('',*,*,#2733,.F.);
#3568=ORIENTED_EDGE('',*,*,#2734,.T.);
#3569=ORIENTED_EDGE('',*,*,#2731,.T.);
#3570=ORIENTED_EDGE('',*,*,#2734,.F.);
#3571=ORIENTED_EDGE('',*,*,#2735,.F.);
#3572=ORIENTED_EDGE('',*,*,#2736,.T.);
#3573=ORIENTED_EDGE('',*,*,#2733,.T.);
#3574=ORIENTED_EDGE('',*,*,#2736,.F.);
#3575=ORIENTED_EDGE('',*,*,#2735,.T.);
#3576=ORIENTED_EDGE('',*,*,#2737,.F.);
#3577=ORIENTED_EDGE('',*,*,#2738,.F.);
#3578=ORIENTED_EDGE('',*,*,#2739,.T.);
#3579=ORIENTED_EDGE('',*,*,#2737,.T.);
#3580=ORIENTED_EDGE('',*,*,#2739,.F.);
#3581=ORIENTED_EDGE('',*,*,#2729,.T.);
#3582=ORIENTED_EDGE('',*,*,#2740,.T.);
#3583=ORIENTED_EDGE('',*,*,#2738,.T.);
#3584=ORIENTED_EDGE('',*,*,#2740,.F.);
#4048=CYLINDRICAL_SURFACE('',#4921,0.65);
#4049=CYLINDRICAL_SURFACE('',#4929,0.3933);
#4210=ADVANCED_FACE('',(#792),#573,.F.);
#4211=ADVANCED_FACE('',(#793),#574,.F.);
#4212=ADVANCED_FACE('',(#794),#575,.F.);
#4213=ADVANCED_FACE('',(#795),#576,.F.);
#4214=ADVANCED_FACE('',(#796),#577,.F.);
#4215=ADVANCED_FACE('',(#797),#578,.F.);
#4216=ADVANCED_FACE('',(#798),#579,.F.);
#4217=ADVANCED_FACE('',(#799),#580,.F.);
#4218=ADVANCED_FACE('',(#800),#581,.F.);
#4219=ADVANCED_FACE('',(#801),#582,.T.);
#4220=ADVANCED_FACE('',(#802),#272,.T.);
#4221=ADVANCED_FACE('',(#803),#4048,.T.);
#4222=ADVANCED_FACE('',(#804),#273,.T.);
#4223=ADVANCED_FACE('',(#805,#461),#583,.T.);
#4224=ADVANCED_FACE('',(#806),#274,.T.);
#4225=ADVANCED_FACE('',(#807),#4049,.T.);
#4342=CLOSED_SHELL('',(#4210,#4211,#4212,#4213,#4214,#4215,#4216,#4217));
#4343=CLOSED_SHELL('',(#4218,#4219,#4220,#4221,#4222,#4223,#4224,#4225));
#4906=AXIS2_PLACEMENT_3D('',#7518,#5824,#5825);
#4907=AXIS2_PLACEMENT_3D('',#7519,#5826,#5827);
#4908=AXIS2_PLACEMENT_3D('',#7528,#5832,#5833);
#4909=AXIS2_PLACEMENT_3D('',#7534,#5837,#5838);
#4910=AXIS2_PLACEMENT_3D('',#7540,#5842,#5843);
#4911=AXIS2_PLACEMENT_3D('',#7546,#5847,#5848);
#4912=AXIS2_PLACEMENT_3D('',#7552,#5852,#5853);
#4913=AXIS2_PLACEMENT_3D('',#7555,#5856,#5857);
#4914=AXIS2_PLACEMENT_3D('',#7556,#5858,#5859);
#4915=AXIS2_PLACEMENT_3D('',#7557,#5860,#5861);
#4916=AXIS2_PLACEMENT_3D('',#7559,#5862,#5863);
#4917=AXIS2_PLACEMENT_3D('',#7560,#5864,#5865);
#4918=AXIS2_PLACEMENT_3D('',#7562,#5866,#5867);
#4919=AXIS2_PLACEMENT_3D('',#7563,#5868,#5869);
#4920=AXIS2_PLACEMENT_3D('',#7565,#5870,#5871);
#4921=AXIS2_PLACEMENT_3D('',#7567,#5873,#5874);
#4922=AXIS2_PLACEMENT_3D('',#7569,#5875,#5876);
#4923=AXIS2_PLACEMENT_3D('',#7571,#5878,#5879);
#4924=AXIS2_PLACEMENT_3D('',#7573,#5880,#5881);
#4925=AXIS2_PLACEMENT_3D('',#7575,#5883,#5884);
#4926=AXIS2_PLACEMENT_3D('',#7577,#5885,#5886);
#4927=AXIS2_PLACEMENT_3D('',#7578,#5887,#5888);
#4928=AXIS2_PLACEMENT_3D('',#7580,#5889,#5890);
#4929=AXIS2_PLACEMENT_3D('',#7582,#5892,#5893);
#5824=DIRECTION('axis',(0.,0.,1.));
#5825=DIRECTION('refdir',(1.,0.,0.));
#5826=DIRECTION('center_axis',(0.866025403784439,0.,-0.5));
#5827=DIRECTION('ref_axis',(0.5,0.,0.866025403784439));
#5828=DIRECTION('',(-0.5,0.,-0.866025403784439));
#5829=DIRECTION('',(0.,-1.,0.));
#5830=DIRECTION('',(0.5,0.,0.866025403784439));
#5831=DIRECTION('',(0.,-1.,0.));
#5832=DIRECTION('center_axis',(1.60246890531964E-16,0.,-1.));
#5833=DIRECTION('ref_axis',(1.,0.,1.60246890531964E-16));
#5834=DIRECTION('',(-1.,0.,-1.60246890531964E-16));
#5835=DIRECTION('',(0.,-1.,0.));
#5836=DIRECTION('',(1.,0.,1.60246890531964E-16));
#5837=DIRECTION('center_axis',(-0.866025403784439,0.,-0.5));
#5838=DIRECTION('ref_axis',(0.5,0.,-0.866025403784439));
#5839=DIRECTION('',(-0.5,0.,0.866025403784439));
#5840=DIRECTION('',(0.,-1.,0.));
#5841=DIRECTION('',(0.5,0.,-0.866025403784439));
#5842=DIRECTION('center_axis',(-0.866025403784439,0.,0.5));
#5843=DIRECTION('ref_axis',(-0.5,0.,-0.866025403784439));
#5844=DIRECTION('',(0.5,0.,0.866025403784439));
#5845=DIRECTION('',(0.,-1.,0.));
#5846=DIRECTION('',(-0.5,0.,-0.866025403784439));
#5847=DIRECTION('center_axis',(-1.60246890531964E-16,0.,1.));
#5848=DIRECTION('ref_axis',(-1.,0.,-1.60246890531964E-16));
#5849=DIRECTION('',(1.,0.,1.60246890531964E-16));
#5850=DIRECTION('',(0.,-1.,0.));
#5851=DIRECTION('',(-1.,0.,-1.60246890531964E-16));
#5852=DIRECTION('center_axis',(0.866025403784439,0.,0.5));
#5853=DIRECTION('ref_axis',(-0.5,0.,0.866025403784439));
#5854=DIRECTION('',(0.5,0.,-0.866025403784439));
#5855=DIRECTION('',(-0.5,0.,0.866025403784439));
#5856=DIRECTION('center_axis',(0.,1.,0.));
#5857=DIRECTION('ref_axis',(1.,0.,0.));
#5858=DIRECTION('center_axis',(0.,-1.,0.));
#5859=DIRECTION('ref_axis',(0.,0.,-1.));
#5860=DIRECTION('center_axis',(0.,1.,0.));
#5861=DIRECTION('ref_axis',(1.,0.,0.));
#5862=DIRECTION('center_axis',(0.,1.,0.));
#5863=DIRECTION('ref_axis',(1.,0.,0.));
#5864=DIRECTION('center_axis',(0.,1.,0.));
#5865=DIRECTION('ref_axis',(0.,0.,1.));
#5866=DIRECTION('center_axis',(0.,-1.,0.));
#5867=DIRECTION('ref_axis',(1.,0.,0.));
#5868=DIRECTION('center_axis',(0.,-1.,0.));
#5869=DIRECTION('ref_axis',(1.,0.,0.));
#5870=DIRECTION('center_axis',(0.,-1.,0.));
#5871=DIRECTION('ref_axis',(1.,0.,0.));
#5872=DIRECTION('',(0.707106781186548,0.707106781186547,8.65956056235493E-17));
#5873=DIRECTION('center_axis',(0.,-1.,0.));
#5874=DIRECTION('ref_axis',(1.,0.,0.));
#5875=DIRECTION('center_axis',(0.,-1.,0.));
#5876=DIRECTION('ref_axis',(1.,0.,0.));
#5877=DIRECTION('',(0.,1.,0.));
#5878=DIRECTION('center_axis',(0.,1.,0.));
#5879=DIRECTION('ref_axis',(1.,0.,0.));
#5880=DIRECTION('center_axis',(0.,-1.,0.));
#5881=DIRECTION('ref_axis',(1.,0.,0.));
#5882=DIRECTION('',(-0.707106781186548,0.707106781186547,-8.65956056235494E-17));
#5883=DIRECTION('center_axis',(0.,-1.,0.));
#5884=DIRECTION('ref_axis',(0.,0.,-1.));
#5885=DIRECTION('center_axis',(0.,-1.,0.));
#5886=DIRECTION('ref_axis',(1.,0.,0.));
#5887=DIRECTION('center_axis',(0.,1.,0.));
#5888=DIRECTION('ref_axis',(1.,0.,0.));
#5889=DIRECTION('center_axis',(0.,1.,0.));
#5890=DIRECTION('ref_axis',(1.,0.,0.));
#5891=DIRECTION('',(-0.447213595499958,0.894427190999916,-5.47678698264203E-17));
#5892=DIRECTION('center_axis',(0.,-1.,0.));
#5893=DIRECTION('ref_axis',(1.,0.,0.));
#5894=DIRECTION('',(0.,1.,0.));
#7518=CARTESIAN_POINT('',(0.,0.,0.));
#7519=CARTESIAN_POINT('Origin',(0.173205080756888,-0.8,-0.3));
#7520=CARTESIAN_POINT('',(0.346410161513775,-0.8,0.));
#7521=CARTESIAN_POINT('',(0.173205080756888,-0.8,-0.3));
#7522=CARTESIAN_POINT('',(0.346410161513775,-0.8,0.));
#7523=CARTESIAN_POINT('',(0.173205080756888,-1.28,-0.3));
#7524=CARTESIAN_POINT('',(0.173205080756888,-0.8,-0.3));
#7525=CARTESIAN_POINT('',(0.346410161513775,-1.28,0.));
#7526=CARTESIAN_POINT('',(0.346410161513775,-1.28,0.));
#7527=CARTESIAN_POINT('',(0.346410161513775,-0.8,0.));
#7528=CARTESIAN_POINT('Origin',(-0.173205080756888,-0.8,-0.3));
#7529=CARTESIAN_POINT('',(-0.173205080756888,-0.8,-0.3));
#7530=CARTESIAN_POINT('',(0.173205080756888,-0.8,-0.3));
#7531=CARTESIAN_POINT('',(-0.173205080756888,-1.28,-0.3));
#7532=CARTESIAN_POINT('',(-0.173205080756888,-0.8,-0.3));
#7533=CARTESIAN_POINT('',(0.173205080756888,-1.28,-0.3));
#7534=CARTESIAN_POINT('Origin',(-0.346410161513775,-0.8,-5.55111512312578E-17));
#7535=CARTESIAN_POINT('',(-0.346410161513775,-0.8,-4.24230095489963E-17));
#7536=CARTESIAN_POINT('',(-0.173205080756888,-0.8,-0.3));
#7537=CARTESIAN_POINT('',(-0.346410161513775,-1.28,-5.55111512312578E-17));
#7538=CARTESIAN_POINT('',(-0.346410161513775,-0.8,-4.24230095489963E-17));
#7539=CARTESIAN_POINT('',(-0.173205080756888,-1.28,-0.3));
#7540=CARTESIAN_POINT('Origin',(-0.173205080756888,-0.8,0.3));
#7541=CARTESIAN_POINT('',(-0.173205080756888,-0.8,0.3));
#7542=CARTESIAN_POINT('',(-0.346410161513775,-0.8,-4.24230095489963E-17));
#7543=CARTESIAN_POINT('',(-0.173205080756888,-1.28,0.3));
#7544=CARTESIAN_POINT('',(-0.173205080756888,-0.8,0.3));
#7545=CARTESIAN_POINT('',(-0.346410161513775,-1.28,-4.24230095489963E-17));
#7546=CARTESIAN_POINT('Origin',(0.173205080756888,-0.8,0.3));
#7547=CARTESIAN_POINT('',(0.173205080756888,-0.8,0.3));
#7548=CARTESIAN_POINT('',(-0.173205080756888,-0.8,0.3));
#7549=CARTESIAN_POINT('',(0.173205080756888,-1.28,0.3));
#7550=CARTESIAN_POINT('',(0.173205080756888,-0.8,0.3));
#7551=CARTESIAN_POINT('',(-0.173205080756888,-1.28,0.3));
#7552=CARTESIAN_POINT('Origin',(0.346410161513775,-0.8,0.));
#7553=CARTESIAN_POINT('',(0.173205080756888,-0.8,0.3));
#7554=CARTESIAN_POINT('',(0.173205080756888,-1.28,0.3));
#7555=CARTESIAN_POINT('Origin',(0.,-0.8,-5.55111512312578E-17));
#7556=CARTESIAN_POINT('Origin',(0.,-1.28,-5.55111512312578E-17));
#7557=CARTESIAN_POINT('Origin',(0.,-2.5,0.));
#7558=CARTESIAN_POINT('',(-0.3933,-2.5,4.81653586104654E-17));
#7559=CARTESIAN_POINT('Origin',(0.,-2.5,0.));
#7560=CARTESIAN_POINT('Origin',(0.6,0.8,0.));
#7561=CARTESIAN_POINT('',(-0.6,0.8,-7.34788079488412E-17));
#7562=CARTESIAN_POINT('Origin',(0.,0.8,0.));
#7563=CARTESIAN_POINT('Origin',(0.,0.775,0.));
#7564=CARTESIAN_POINT('',(-0.65,0.75,-7.9602041944578E-17));
#7565=CARTESIAN_POINT('Origin',(0.,0.75,0.));
#7566=CARTESIAN_POINT('',(-0.625,0.775,-7.65404249467096E-17));
#7567=CARTESIAN_POINT('Origin',(0.,0.39,0.));
#7568=CARTESIAN_POINT('',(-0.65,0.0299999999999998,-7.9602041944578E-17));
#7569=CARTESIAN_POINT('Origin',(0.,0.0299999999999998,0.));
#7570=CARTESIAN_POINT('',(-0.65,0.39,-7.9602041944578E-17));
#7571=CARTESIAN_POINT('Origin',(0.,0.0150000000000001,0.));
#7572=CARTESIAN_POINT('',(-0.62,5.89805981832114E-17,-7.59281015471359E-17));
#7573=CARTESIAN_POINT('Origin',(0.,0.,0.));
#7574=CARTESIAN_POINT('',(-0.635,0.0150000000000001,-7.77650717458569E-17));
#7575=CARTESIAN_POINT('Origin',(0.42,0.,0.));
#7576=CARTESIAN_POINT('',(-0.42,-3.46944695195361E-18,-5.14351655641888E-17));
#7577=CARTESIAN_POINT('Origin',(0.,0.,0.));
#7578=CARTESIAN_POINT('Origin',(0.,-0.02,0.));
#7579=CARTESIAN_POINT('',(-0.3933,-0.0534000000000001,4.81653586104654E-17));
#7580=CARTESIAN_POINT('Origin',(0.,-0.0534000000000001,0.));
#7581=CARTESIAN_POINT('',(-0.41,-0.02,-5.02105187650415E-17));
#7582=CARTESIAN_POINT('Origin',(0.,-1.48,0.));
#7583=CARTESIAN_POINT('',(-0.3933,-1.48,-4.81653586104654E-17));
#8333=UNCERTAINTY_MEASURE_WITH_UNIT(LENGTH_MEASURE(0.001),#8378,
'DISTANCE_ACCURACY_VALUE',
'Maximum model space distance between geometric entities at asserted c
onnectivities');
#8345=UNCERTAINTY_MEASURE_WITH_UNIT(LENGTH_MEASURE(0.001),#8378,
'DISTANCE_ACCURACY_VALUE',
'Maximum model space distance between geometric entities at asserted c
onnectivities');
#8365=(
GEOMETRIC_REPRESENTATION_CONTEXT(3)
GLOBAL_UNCERTAINTY_ASSIGNED_CONTEXT((#8333))
GLOBAL_UNIT_ASSIGNED_CONTEXT((#8378,#8380,#8381))
REPRESENTATION_CONTEXT('','3D')
);
#8377=(
GEOMETRIC_REPRESENTATION_CONTEXT(3)
GLOBAL_UNCERTAINTY_ASSIGNED_CONTEXT((#8345))
GLOBAL_UNIT_ASSIGNED_CONTEXT((#8378,#8380,#8381))
REPRESENTATION_CONTEXT('','3D')
);
#8378=(
LENGTH_UNIT()
NAMED_UNIT(*)
SI_UNIT(.CENTI.,.METRE.)
);
#8380=(
NAMED_UNIT(*)
PLANE_ANGLE_UNIT()
SI_UNIT($,.RADIAN.)
);
#8381=(
NAMED_UNIT(*)
SI_UNIT($,.STERADIAN.)
SOLID_ANGLE_UNIT()
);
#8401=SHAPE_DEFINITION_REPRESENTATION(#8434,#8516);
#8434=PRODUCT_DEFINITION_SHAPE('',$,#8548);
#8516=SHAPE_REPRESENTATION('',(#4906),#8365);
#8528=PRODUCT_DEFINITION_CONTEXT('part definition',#8623,'design');
#8548=PRODUCT_DEFINITION('M8x25 Bolt','M8x25 Bolt',#8579,#8528);
#8579=PRODUCT_DEFINITION_FORMATION('',$,#8644);
#8623=APPLICATION_CONTEXT(
'Core Data for Automotive Mechanical Design Process');
#8624=PRODUCT_CONTEXT('part definition',#8623,'mechanical');
#8644=PRODUCT('M8x25 Bolt','M8x25 Bolt','M8x25 Bolt',(#8624));
#8719=COLOUR_RGB('Black',0.12,0.14,0.17);
#8720=FILL_AREA_STYLE_COLOUR('',#8719);
#8721=FILL_AREA_STYLE('',(#8720));
#8722=SURFACE_STYLE_FILL_AREA(#8721);
#8723=SURFACE_SIDE_STYLE('',(#8722));
#8724=SURFACE_STYLE_USAGE(.BOTH.,#8723);
#8725=PRESENTATION_STYLE_ASSIGNMENT((#8724));
ENDSEC;
END-ISO-10303-21;
